ISO-10303-21;
HEADER;
/* Generated by software containing ST-Developer
 * from STEP Tools, Inc. (www.steptools.com) 
 */
/* OPTION: using custom renumber hook */

FILE_DESCRIPTION(
/* description */ ('STEP AP242 Edition 2', 'CAx-IF Rec.Pracs.---Representation and Presentation of Product Manufa
cturing Information (PMI)---4.0---2014-10-13', 'CAx-IF Rec.Pracs.---3D Tessellated Geometry---0.4---2014-09-14', '2;1', 'CAx-IF Rec.Pracs.---User Defined Attributes---1.5---2016-08-15'),
/* implementation_level */ '2;1');

FILE_NAME(
/* name */ 'Part 1__PD10222.step',
/* time_stamp */ '2026-10-09T13:59:33Z',
/* author */ (''),
/* organization */ (''),
/* preprocessor_version */ 'ST-DEVELOPER v20',
/* originating_system */ 'ONSHAPE BY PTC INC, 1.221',
/* authorisation */ '  ');

FILE_SCHEMA (('AP242_MANAGED_MODEL_BASED_3D_ENGINEERING_MIM_LF { 1 0 10303 442 3 1 4 }'));
ENDSEC;

DATA;
#286=LINE('',#9909,#570);
#287=LINE('',#9913,#571);
#288=LINE('',#9920,#572);
#289=LINE('',#9924,#573);
#290=LINE('',#9930,#574);
#291=LINE('',#9931,#575);
#292=LINE('',#9933,#576);
#293=LINE('',#9935,#577);
#570=VECTOR('',#8156,1.);
#571=VECTOR('',#8159,1.);
#572=VECTOR('',#8166,1.);
#573=VECTOR('',#8169,1.);
#574=VECTOR('',#8176,1.);
#575=VECTOR('',#8177,1.);
#576=VECTOR('',#8180,1.);
#577=VECTOR('',#8183,1.);
#681=SHAPE_REPRESENTATION_RELATIONSHIP('','',#5700,#695);
#695=ADVANCED_BREP_SHAPE_REPRESENTATION('',(#5668),#10154);
#769=PLANE('',#6401);
#770=PLANE('',#6406);
#771=PLANE('',#6412);
#772=PLANE('',#6414);
#2164=ORIENTED_EDGE('',*,*,#3019,.F.);
#2165=ORIENTED_EDGE('',*,*,#3020,.T.);
#2166=ORIENTED_EDGE('',*,*,#3021,.T.);
#2167=ORIENTED_EDGE('',*,*,#3022,.T.);
#2168=ORIENTED_EDGE('',*,*,#3023,.T.);
#2169=ORIENTED_EDGE('',*,*,#3024,.F.);
#2170=ORIENTED_EDGE('',*,*,#3025,.F.);
#2171=ORIENTED_EDGE('',*,*,#3026,.F.);
#2172=ORIENTED_EDGE('',*,*,#3027,.F.);
#2173=ORIENTED_EDGE('',*,*,#3028,.F.);
#2174=ORIENTED_EDGE('',*,*,#3029,.T.);
#2175=ORIENTED_EDGE('',*,*,#3030,.T.);
#2176=ORIENTED_EDGE('',*,*,#3025,.T.);
#2177=ORIENTED_EDGE('',*,*,#3031,.F.);
#2178=ORIENTED_EDGE('',*,*,#3020,.F.);
#2179=ORIENTED_EDGE('',*,*,#3032,.T.);
#2180=ORIENTED_EDGE('',*,*,#3028,.T.);
#2181=ORIENTED_EDGE('',*,*,#3033,.F.);
#2182=ORIENTED_EDGE('',*,*,#3021,.F.);
#2183=ORIENTED_EDGE('',*,*,#3031,.T.);
#2184=ORIENTED_EDGE('',*,*,#3027,.T.);
#2185=ORIENTED_EDGE('',*,*,#3034,.F.);
#2186=ORIENTED_EDGE('',*,*,#3022,.F.);
#2187=ORIENTED_EDGE('',*,*,#3033,.T.);
#2188=ORIENTED_EDGE('',*,*,#3026,.T.);
#2189=ORIENTED_EDGE('',*,*,#3032,.F.);
#2190=ORIENTED_EDGE('',*,*,#3023,.F.);
#2191=ORIENTED_EDGE('',*,*,#3034,.T.);
#2192=ORIENTED_EDGE('',*,*,#3019,.T.);
#2193=ORIENTED_EDGE('',*,*,#3029,.F.);
#2194=ORIENTED_EDGE('',*,*,#3024,.T.);
#2195=ORIENTED_EDGE('',*,*,#3030,.F.);
#3019=EDGE_CURVE('',#3581,#3581,#4058,.T.);
#3020=EDGE_CURVE('',#3582,#3583,#4059,.T.);
#3021=EDGE_CURVE('',#3583,#3584,#286,.T.);
#3022=EDGE_CURVE('',#3584,#3585,#4060,.T.);
#3023=EDGE_CURVE('',#3585,#3582,#287,.T.);
#3024=EDGE_CURVE('',#3586,#3586,#4061,.T.);
#3025=EDGE_CURVE('',#3587,#3588,#4062,.T.);
#3026=EDGE_CURVE('',#3589,#3587,#288,.T.);
#3027=EDGE_CURVE('',#3590,#3589,#4063,.T.);
#3028=EDGE_CURVE('',#3588,#3590,#289,.T.);
#3029=EDGE_CURVE('',#3591,#3591,#4064,.T.);
#3030=EDGE_CURVE('',#3592,#3592,#4065,.T.);
#3031=EDGE_CURVE('',#3583,#3588,#290,.T.);
#3032=EDGE_CURVE('',#3582,#3587,#291,.T.);
#3033=EDGE_CURVE('',#3584,#3590,#292,.T.);
#3034=EDGE_CURVE('',#3585,#3589,#293,.T.);
#3581=VERTEX_POINT('',#9905);
#3582=VERTEX_POINT('',#9907);
#3583=VERTEX_POINT('',#9908);
#3584=VERTEX_POINT('',#9910);
#3585=VERTEX_POINT('',#9912);
#3586=VERTEX_POINT('',#9915);
#3587=VERTEX_POINT('',#9918);
#3588=VERTEX_POINT('',#9919);
#3589=VERTEX_POINT('',#9921);
#3590=VERTEX_POINT('',#9923);
#3591=VERTEX_POINT('',#9926);
#3592=VERTEX_POINT('',#9928);
#4058=CIRCLE('',#6402,0.0015);
#4059=CIRCLE('',#6403,0.002);
#4060=CIRCLE('',#6404,0.002);
#4061=CIRCLE('',#6405,0.0015);
#4062=CIRCLE('',#6407,0.002);
#4063=CIRCLE('',#6408,0.002);
#4064=CIRCLE('',#6409,0.0015);
#4065=CIRCLE('',#6410,0.0015);
#4474=EDGE_LOOP('',(#2164));
#4475=EDGE_LOOP('',(#2165,#2166,#2167,#2168));
#4476=EDGE_LOOP('',(#2169));
#4477=EDGE_LOOP('',(#2170,#2171,#2172,#2173));
#4478=EDGE_LOOP('',(#2174));
#4479=EDGE_LOOP('',(#2175));
#4480=EDGE_LOOP('',(#2176,#2177,#2178,#2179));
#4481=EDGE_LOOP('',(#2180,#2181,#2182,#2183));
#4482=EDGE_LOOP('',(#2184,#2185,#2186,#2187));
#4483=EDGE_LOOP('',(#2188,#2189,#2190,#2191));
#4484=EDGE_LOOP('',(#2192));
#4485=EDGE_LOOP('',(#2193));
#4486=EDGE_LOOP('',(#2194));
#4487=EDGE_LOOP('',(#2195));
#4922=FACE_BOUND('',#4474,.T.);
#4923=FACE_BOUND('',#4475,.T.);
#4924=FACE_BOUND('',#4476,.T.);
#4925=FACE_BOUND('',#4477,.T.);
#4926=FACE_BOUND('',#4478,.T.);
#4927=FACE_BOUND('',#4479,.T.);
#4928=FACE_BOUND('',#4480,.T.);
#4929=FACE_BOUND('',#4481,.T.);
#4930=FACE_BOUND('',#4482,.T.);
#4931=FACE_BOUND('',#4483,.T.);
#4932=FACE_BOUND('',#4484,.T.);
#4933=FACE_BOUND('',#4485,.T.);
#4934=FACE_BOUND('',#4486,.T.);
#4935=FACE_BOUND('',#4487,.T.);
#5197=CYLINDRICAL_SURFACE('',#6411,0.002);
#5198=CYLINDRICAL_SURFACE('',#6413,0.002);
#5199=CYLINDRICAL_SURFACE('',#6415,0.0015);
#5200=CYLINDRICAL_SURFACE('',#6416,0.0015);
#5488=ADVANCED_FACE('',(#4922,#4923,#4924),#769,.T.);
#5489=ADVANCED_FACE('',(#4925,#4926,#4927),#770,.F.);
#5490=ADVANCED_FACE('',(#4928),#5197,.T.);
#5491=ADVANCED_FACE('',(#4929),#771,.F.);
#5492=ADVANCED_FACE('',(#4930),#5198,.T.);
#5493=ADVANCED_FACE('',(#4931),#772,.F.);
#5494=ADVANCED_FACE('',(#4932,#4933),#5199,.F.);
#5495=ADVANCED_FACE('',(#4934,#4935),#5200,.F.);
#5549=CLOSED_SHELL('',(#5488,#5489,#5490,#5491,#5492,#5493,#5494,#5495));
#5563=STYLED_ITEM('',(#5577),#5668);
#5577=PRESENTATION_STYLE_ASSIGNMENT((#5591));
#5591=SURFACE_STYLE_USAGE(.BOTH.,#5605);
#5605=SURFACE_SIDE_STYLE('',(#5619));
#5619=SURFACE_STYLE_FILL_AREA(#5633);
#5633=FILL_AREA_STYLE('',(#5647));
#5647=FILL_AREA_STYLE_COLOUR('',#5653);
#5653=COLOUR_RGB('', 0.40784314, 0.44705882, 0.49803922);
#5668=MANIFOLD_SOLID_BREP('Part 1',#5549);
#5684=SHAPE_DEFINITION_REPRESENTATION(#10202,#5700);
#5700=SHAPE_REPRESENTATION('Part 1',(#5704),#10154);
#5704=AXIS2_PLACEMENT_3D('',#8391,#6505,#6506);
#6401=AXIS2_PLACEMENT_3D('',#9903,#8150,#8151);
#6402=AXIS2_PLACEMENT_3D('',#9904,#8152,#8153);
#6403=AXIS2_PLACEMENT_3D('',#9906,#8154,#8155);
#6404=AXIS2_PLACEMENT_3D('',#9911,#8157,#8158);
#6405=AXIS2_PLACEMENT_3D('',#9914,#8160,#8161);
#6406=AXIS2_PLACEMENT_3D('',#9916,#8162,#8163);
#6407=AXIS2_PLACEMENT_3D('',#9917,#8164,#8165);
#6408=AXIS2_PLACEMENT_3D('',#9922,#8167,#8168);
#6409=AXIS2_PLACEMENT_3D('',#9925,#8170,#8171);
#6410=AXIS2_PLACEMENT_3D('',#9927,#8172,#8173);
#6411=AXIS2_PLACEMENT_3D('',#9929,#8174,#8175);
#6412=AXIS2_PLACEMENT_3D('',#9932,#8178,#8179);
#6413=AXIS2_PLACEMENT_3D('',#9934,#8181,#8182);
#6414=AXIS2_PLACEMENT_3D('',#9936,#8184,#8185);
#6415=AXIS2_PLACEMENT_3D('',#9937,#8186,#8187);
#6416=AXIS2_PLACEMENT_3D('',#9938,#8188,#8189);
#6505=DIRECTION('',(0.,0.,1.));
#6506=DIRECTION('',(1.,0.,0.));
#8150=DIRECTION('',(0.,1.,0.));
#8151=DIRECTION('',(0.,0.,1.));
#8152=DIRECTION('',(0.,1.,0.));
#8153=DIRECTION('',(0.,0.,1.));
#8154=DIRECTION('',(0.,1.,0.));
#8155=DIRECTION('',(0.,0.,1.));
#8156=DIRECTION('',(1.,0.,0.));
#8157=DIRECTION('',(0.,1.,0.));
#8158=DIRECTION('',(0.,0.,1.));
#8159=DIRECTION('',(-1.,0.,0.));
#8160=DIRECTION('',(0.,1.,0.));
#8161=DIRECTION('',(0.,0.,1.));
#8162=DIRECTION('',(0.,1.,0.));
#8163=DIRECTION('',(0.,0.,1.));
#8164=DIRECTION('',(0.,1.,0.));
#8165=DIRECTION('',(0.,0.,1.));
#8166=DIRECTION('',(-1.,0.,0.));
#8167=DIRECTION('',(0.,1.,0.));
#8168=DIRECTION('',(0.,0.,1.));
#8169=DIRECTION('',(1.,0.,0.));
#8170=DIRECTION('',(0.,1.,0.));
#8171=DIRECTION('',(0.,0.,1.));
#8172=DIRECTION('',(0.,1.,0.));
#8173=DIRECTION('',(0.,0.,1.));
#8174=DIRECTION('',(0.,-1.,0.));
#8175=DIRECTION('',(0.,0.,-1.));
#8176=DIRECTION('',(0.,-1.,0.));
#8177=DIRECTION('',(0.,-1.,0.));
#8178=DIRECTION('',(0.,0.,-1.));
#8179=DIRECTION('',(-1.,0.,0.));
#8180=DIRECTION('',(0.,-1.,0.));
#8181=DIRECTION('',(0.,-1.,0.));
#8182=DIRECTION('',(0.,0.,-1.));
#8183=DIRECTION('',(0.,-1.,0.));
#8184=DIRECTION('',(0.,0.,1.));
#8185=DIRECTION('',(1.,0.,0.));
#8186=DIRECTION('',(0.,-1.,0.));
#8187=DIRECTION('',(0.,0.,-1.));
#8188=DIRECTION('',(0.,-1.,0.));
#8189=DIRECTION('',(0.,0.,-1.));
#8391=CARTESIAN_POINT('',(0.,0.,0.));
#9903=CARTESIAN_POINT('',(-0.012585,0.001,0.));
#9904=CARTESIAN_POINT('',(-0.012585,0.001,0.));
#9905=CARTESIAN_POINT('',(-0.012585,0.001,0.0015));
#9906=CARTESIAN_POINT('',(-0.012585,0.001,0.));
#9907=CARTESIAN_POINT('',(-0.012585,0.001,-0.002));
#9908=CARTESIAN_POINT('',(-0.012585,0.001,0.002));
#9909=CARTESIAN_POINT('',(-0.012585,0.001,0.002));
#9910=CARTESIAN_POINT('',(0.012585,0.001,0.002));
#9911=CARTESIAN_POINT('',(0.012585,0.001,0.));
#9912=CARTESIAN_POINT('',(0.012585,0.001,-0.002));
#9913=CARTESIAN_POINT('',(-0.012585,0.001,-0.002));
#9914=CARTESIAN_POINT('',(0.012585,0.001,0.));
#9915=CARTESIAN_POINT('',(0.012585,0.001,0.0015));
#9916=CARTESIAN_POINT('',(-0.012585,0.,0.));
#9917=CARTESIAN_POINT('',(-0.012585,0.,0.));
#9918=CARTESIAN_POINT('',(-0.012585,0.,-0.002));
#9919=CARTESIAN_POINT('',(-0.012585,0.,0.002));
#9920=CARTESIAN_POINT('',(-0.012585,0.,-0.002));
#9921=CARTESIAN_POINT('',(0.012585,0.,-0.002));
#9922=CARTESIAN_POINT('',(0.012585,0.,0.));
#9923=CARTESIAN_POINT('',(0.012585,0.,0.002));
#9924=CARTESIAN_POINT('',(-0.012585,0.,0.002));
#9925=CARTESIAN_POINT('',(-0.012585,0.,0.));
#9926=CARTESIAN_POINT('',(-0.012585,0.,0.0015));
#9927=CARTESIAN_POINT('',(0.012585,0.,0.));
#9928=CARTESIAN_POINT('',(0.012585,0.,0.0015));
#9929=CARTESIAN_POINT('',(-0.012585,0.001,0.));
#9930=CARTESIAN_POINT('',(-0.012585,0.001,0.002));
#9931=CARTESIAN_POINT('',(-0.012585,0.001,-0.002));
#9932=CARTESIAN_POINT('',(-0.012585,0.001,0.002));
#9933=CARTESIAN_POINT('',(0.012585,0.001,0.002));
#9934=CARTESIAN_POINT('',(0.012585,0.001,0.));
#9935=CARTESIAN_POINT('',(0.012585,0.001,-0.002));
#9936=CARTESIAN_POINT('',(-0.012585,0.001,-0.002));
#9937=CARTESIAN_POINT('',(-0.012585,0.001,0.));
#9938=CARTESIAN_POINT('',(0.012585,0.001,0.));
#10141=MECHANICAL_DESIGN_GEOMETRIC_PRESENTATION_REPRESENTATION('',(#5563),#10142);
#10142=(
GEOMETRIC_REPRESENTATION_CONTEXT(3)
GLOBAL_UNCERTAINTY_ASSIGNED_CONTEXT((#10158))
GLOBAL_UNIT_ASSIGNED_CONTEXT((#10176,#10175,#10174))
REPRESENTATION_CONTEXT('MAS-674','TOP_LEVEL_ASSEMBLY_PART')
);
#10154=(
GEOMETRIC_REPRESENTATION_CONTEXT(3)
GLOBAL_UNCERTAINTY_ASSIGNED_CONTEXT((#10170))
GLOBAL_UNIT_ASSIGNED_CONTEXT((#10176,#10175,#10174))
REPRESENTATION_CONTEXT('Part 1','COMPONENT_PART')
);
#10158=UNCERTAINTY_MEASURE_WITH_UNIT(LENGTH_MEASURE(1.E-8),#10176,
'DISTANCE_ACCURACY_VALUE','Maximum Tolerance applied to model');
#10170=UNCERTAINTY_MEASURE_WITH_UNIT(LENGTH_MEASURE(1.E-8),#10176,
'DISTANCE_ACCURACY_VALUE','Maximum Tolerance applied to model');
#10174=(
NAMED_UNIT(*)
SI_UNIT($,.STERADIAN.)
SOLID_ANGLE_UNIT()
);
#10175=(
NAMED_UNIT(*)
PLANE_ANGLE_UNIT()
SI_UNIT($,.RADIAN.)
);
#10176=(
LENGTH_UNIT()
NAMED_UNIT(*)
SI_UNIT($,.METRE.)
);
#10202=PRODUCT_DEFINITION_SHAPE('','',#10222);
#10222=PRODUCT_DEFINITION('','',#10254,#10238);
#10238=PRODUCT_DEFINITION_CONTEXT('',#10323,'design');
#10254=PRODUCT_DEFINITION_FORMATION_WITH_SPECIFIED_SOURCE('','',#10286,
 .NOT_KNOWN.);
#10286=PRODUCT('Part 1','Part 1','Part 1',(#10318));
#10318=PRODUCT_CONTEXT('',#10323,'mechanical');
#10323=APPLICATION_CONTEXT('managed model based 3d engineering');
ENDSEC;
END-ISO-10303-21;
